ISO-10303-21;
HEADER;
/* Generated by software containing ST-Developer
 * from STEP Tools, Inc. (www.steptools.com) 
 */

FILE_DESCRIPTION(
/* description */ ('Self-centering screw clamp'),
/* implementation_level */ '2;1');

FILE_NAME(
/* name */ 'Socket Set Screw - M4x6.step',
/* time_stamp */ '2026-10-28T03:25:31-07:00',
/* author */ (''),
/* organization */ (''),
/* preprocessor_version */ 'ST-DEVELOPER v20.2',
/* originating_system */ 'Autodesk Translation Framework v15.17.0.0',
/* authorisation */ '');

FILE_SCHEMA (('AUTOMOTIVE_DESIGN { 1 0 10303 214 3 1 1 }'));
ENDSEC;

DATA;
#10=MECHANICAL_DESIGN_GEOMETRIC_PRESENTATION_REPRESENTATION('',(#671),#16799);
#496=CONICAL_SURFACE('',#10681,0.185,0.785398163397449);
#497=CONICAL_SURFACE('',#10685,0.1625,0.785398163397449);
#582=SHAPE_REPRESENTATION_RELATIONSHIP('SRR','None',#17060,#623);
#623=ADVANCED_BREP_SHAPE_REPRESENTATION('',(#717),#16798);
#671=STYLED_ITEM('',(#17333),#717);
#717=MANIFOLD_SOLID_BREP('Body1',#9124);
#1013=FACE_BOUND('',#2572,.T.);
#1264=PLANE('',#10672);
#1265=PLANE('',#10673);
#1266=PLANE('',#10674);
#1267=PLANE('',#10675);
#1268=PLANE('',#10676);
#1269=PLANE('',#10677);
#1270=PLANE('',#10678);
#1271=PLANE('',#10679);
#1272=PLANE('',#10687);
#1765=FACE_OUTER_BOUND('',#2564,.T.);
#1766=FACE_OUTER_BOUND('',#2565,.T.);
#1767=FACE_OUTER_BOUND('',#2566,.T.);
#1768=FACE_OUTER_BOUND('',#2567,.T.);
#1769=FACE_OUTER_BOUND('',#2568,.T.);
#1770=FACE_OUTER_BOUND('',#2569,.T.);
#1771=FACE_OUTER_BOUND('',#2570,.T.);
#1772=FACE_OUTER_BOUND('',#2571,.T.);
#1773=FACE_OUTER_BOUND('',#2573,.T.);
#1774=FACE_OUTER_BOUND('',#2574,.T.);
#1775=FACE_OUTER_BOUND('',#2575,.T.);
#1776=FACE_OUTER_BOUND('',#2576,.T.);
#2564=EDGE_LOOP('',(#8307,#8308,#8309,#8310));
#2565=EDGE_LOOP('',(#8311,#8312,#8313,#8314));
#2566=EDGE_LOOP('',(#8315,#8316,#8317,#8318));
#2567=EDGE_LOOP('',(#8319,#8320,#8321,#8322));
#2568=EDGE_LOOP('',(#8323,#8324,#8325,#8326));
#2569=EDGE_LOOP('',(#8327,#8328,#8329,#8330));
#2570=EDGE_LOOP('',(#8331,#8332,#8333,#8334,#8335,#8336));
#2571=EDGE_LOOP('',(#8337));
#2572=EDGE_LOOP('',(#8338,#8339,#8340,#8341,#8342,#8343));
#2573=EDGE_LOOP('',(#8344,#8345,#8346,#8347));
#2574=EDGE_LOOP('',(#8348,#8349,#8350,#8351));
#2575=EDGE_LOOP('',(#8352,#8353,#8354,#8355));
#2576=EDGE_LOOP('',(#8356));
#3129=LINE('',#16588,#3702);
#3130=LINE('',#16590,#3703);
#3131=LINE('',#16592,#3704);
#3132=LINE('',#16593,#3705);
#3133=LINE('',#16596,#3706);
#3134=LINE('',#16598,#3707);
#3135=LINE('',#16599,#3708);
#3136=LINE('',#16602,#3709);
#3137=LINE('',#16604,#3710);
#3138=LINE('',#16605,#3711);
#3139=LINE('',#16608,#3712);
#3140=LINE('',#16610,#3713);
#3141=LINE('',#16611,#3714);
#3142=LINE('',#16614,#3715);
#3143=LINE('',#16616,#3716);
#3144=LINE('',#16617,#3717);
#3145=LINE('',#16619,#3718);
#3146=LINE('',#16620,#3719);
#3147=LINE('',#16628,#3720);
#3148=LINE('',#16632,#3721);
#3149=LINE('',#16636,#3722);
#3702=VECTOR('',#13496,1.);
#3703=VECTOR('',#13497,1.);
#3704=VECTOR('',#13498,1.);
#3705=VECTOR('',#13499,1.);
#3706=VECTOR('',#13502,1.);
#3707=VECTOR('',#13503,1.);
#3708=VECTOR('',#13504,1.);
#3709=VECTOR('',#13507,1.);
#3710=VECTOR('',#13508,1.);
#3711=VECTOR('',#13509,1.);
#3712=VECTOR('',#13512,1.);
#3713=VECTOR('',#13513,1.);
#3714=VECTOR('',#13514,1.);
#3715=VECTOR('',#13517,1.);
#3716=VECTOR('',#13518,1.);
#3717=VECTOR('',#13519,1.);
#3718=VECTOR('',#13522,1.);
#3719=VECTOR('',#13523,1.);
#3720=VECTOR('',#13534,0.185);
#3721=VECTOR('',#13539,0.2);
#3722=VECTOR('',#13544,0.1625);
#4229=CIRCLE('',#10680,0.17);
#4230=CIRCLE('',#10682,0.1954);
#4231=CIRCLE('',#10684,0.1954);
#4232=CIRCLE('',#10686,0.125);
#4960=VERTEX_POINT('',#16586);
#4961=VERTEX_POINT('',#16587);
#4962=VERTEX_POINT('',#16589);
#4963=VERTEX_POINT('',#16591);
#4964=VERTEX_POINT('',#16595);
#4965=VERTEX_POINT('',#16597);
#4966=VERTEX_POINT('',#16601);
#4967=VERTEX_POINT('',#16603);
#4968=VERTEX_POINT('',#16607);
#4969=VERTEX_POINT('',#16609);
#4970=VERTEX_POINT('',#16613);
#4971=VERTEX_POINT('',#16615);
#4972=VERTEX_POINT('',#16623);
#4973=VERTEX_POINT('',#16626);
#4974=VERTEX_POINT('',#16630);
#4975=VERTEX_POINT('',#16634);
#6078=EDGE_CURVE('',#4960,#4961,#3129,.T.);
#6079=EDGE_CURVE('',#4960,#4962,#3130,.T.);
#6080=EDGE_CURVE('',#4962,#4963,#3131,.T.);
#6081=EDGE_CURVE('',#4961,#4963,#3132,.T.);
#6082=EDGE_CURVE('',#4964,#4960,#3133,.T.);
#6083=EDGE_CURVE('',#4964,#4965,#3134,.T.);
#6084=EDGE_CURVE('',#4965,#4962,#3135,.T.);
#6085=EDGE_CURVE('',#4966,#4964,#3136,.T.);
#6086=EDGE_CURVE('',#4966,#4967,#3137,.T.);
#6087=EDGE_CURVE('',#4967,#4965,#3138,.T.);
#6088=EDGE_CURVE('',#4968,#4966,#3139,.T.);
#6089=EDGE_CURVE('',#4968,#4969,#3140,.T.);
#6090=EDGE_CURVE('',#4969,#4967,#3141,.T.);
#6091=EDGE_CURVE('',#4970,#4968,#3142,.T.);
#6092=EDGE_CURVE('',#4970,#4971,#3143,.T.);
#6093=EDGE_CURVE('',#4971,#4969,#3144,.T.);
#6094=EDGE_CURVE('',#4961,#4970,#3145,.T.);
#6095=EDGE_CURVE('',#4963,#4971,#3146,.T.);
#6096=EDGE_CURVE('',#4972,#4972,#4229,.T.);
#6097=EDGE_CURVE('',#4973,#4973,#4230,.T.);
#6098=EDGE_CURVE('',#4973,#4972,#3147,.T.);
#6099=EDGE_CURVE('',#4974,#4974,#4231,.F.);
#6100=EDGE_CURVE('',#4974,#4973,#3148,.T.);
#6101=EDGE_CURVE('',#4975,#4975,#4232,.T.);
#6102=EDGE_CURVE('',#4975,#4974,#3149,.T.);
#8307=ORIENTED_EDGE('',*,*,#6078,.F.);
#8308=ORIENTED_EDGE('',*,*,#6079,.T.);
#8309=ORIENTED_EDGE('',*,*,#6080,.T.);
#8310=ORIENTED_EDGE('',*,*,#6081,.F.);
#8311=ORIENTED_EDGE('',*,*,#6082,.F.);
#8312=ORIENTED_EDGE('',*,*,#6083,.T.);
#8313=ORIENTED_EDGE('',*,*,#6084,.T.);
#8314=ORIENTED_EDGE('',*,*,#6079,.F.);
#8315=ORIENTED_EDGE('',*,*,#6085,.F.);
#8316=ORIENTED_EDGE('',*,*,#6086,.T.);
#8317=ORIENTED_EDGE('',*,*,#6087,.T.);
#8318=ORIENTED_EDGE('',*,*,#6083,.F.);
#8319=ORIENTED_EDGE('',*,*,#6088,.F.);
#8320=ORIENTED_EDGE('',*,*,#6089,.T.);
#8321=ORIENTED_EDGE('',*,*,#6090,.T.);
#8322=ORIENTED_EDGE('',*,*,#6086,.F.);
#8323=ORIENTED_EDGE('',*,*,#6091,.F.);
#8324=ORIENTED_EDGE('',*,*,#6092,.T.);
#8325=ORIENTED_EDGE('',*,*,#6093,.T.);
#8326=ORIENTED_EDGE('',*,*,#6089,.F.);
#8327=ORIENTED_EDGE('',*,*,#6094,.F.);
#8328=ORIENTED_EDGE('',*,*,#6081,.T.);
#8329=ORIENTED_EDGE('',*,*,#6095,.T.);
#8330=ORIENTED_EDGE('',*,*,#6092,.F.);
#8331=ORIENTED_EDGE('',*,*,#6095,.F.);
#8332=ORIENTED_EDGE('',*,*,#6080,.F.);
#8333=ORIENTED_EDGE('',*,*,#6084,.F.);
#8334=ORIENTED_EDGE('',*,*,#6087,.F.);
#8335=ORIENTED_EDGE('',*,*,#6090,.F.);
#8336=ORIENTED_EDGE('',*,*,#6093,.F.);
#8337=ORIENTED_EDGE('',*,*,#6096,.F.);
#8338=ORIENTED_EDGE('',*,*,#6078,.T.);
#8339=ORIENTED_EDGE('',*,*,#6094,.T.);
#8340=ORIENTED_EDGE('',*,*,#6091,.T.);
#8341=ORIENTED_EDGE('',*,*,#6088,.T.);
#8342=ORIENTED_EDGE('',*,*,#6085,.T.);
#8343=ORIENTED_EDGE('',*,*,#6082,.T.);
#8344=ORIENTED_EDGE('',*,*,#6097,.F.);
#8345=ORIENTED_EDGE('',*,*,#6098,.T.);
#8346=ORIENTED_EDGE('',*,*,#6096,.T.);
#8347=ORIENTED_EDGE('',*,*,#6098,.F.);
#8348=ORIENTED_EDGE('',*,*,#6099,.F.);
#8349=ORIENTED_EDGE('',*,*,#6100,.T.);
#8350=ORIENTED_EDGE('',*,*,#6097,.T.);
#8351=ORIENTED_EDGE('',*,*,#6100,.F.);
#8352=ORIENTED_EDGE('',*,*,#6101,.F.);
#8353=ORIENTED_EDGE('',*,*,#6102,.T.);
#8354=ORIENTED_EDGE('',*,*,#6099,.T.);
#8355=ORIENTED_EDGE('',*,*,#6102,.F.);
#8356=ORIENTED_EDGE('',*,*,#6101,.T.);
#8570=CYLINDRICAL_SURFACE('',#10683,0.1954);
#9063=ADVANCED_FACE('',(#1765),#1264,.F.);
#9064=ADVANCED_FACE('',(#1766),#1265,.F.);
#9065=ADVANCED_FACE('',(#1767),#1266,.F.);
#9066=ADVANCED_FACE('',(#1768),#1267,.F.);
#9067=ADVANCED_FACE('',(#1769),#1268,.F.);
#9068=ADVANCED_FACE('',(#1770),#1269,.F.);
#9069=ADVANCED_FACE('',(#1771),#1270,.F.);
#9070=ADVANCED_FACE('',(#1772,#1013),#1271,.T.);
#9071=ADVANCED_FACE('',(#1773),#496,.T.);
#9072=ADVANCED_FACE('',(#1774),#8570,.T.);
#9073=ADVANCED_FACE('',(#1775),#497,.T.);
#9074=ADVANCED_FACE('',(#1776),#1272,.T.);
#9124=CLOSED_SHELL('',(#9063,#9064,#9065,#9066,#9067,#9068,#9069,#9070,
#9071,#9072,#9073,#9074));
#10671=AXIS2_PLACEMENT_3D('',#16584,#13492,#13493);
#10672=AXIS2_PLACEMENT_3D('',#16585,#13494,#13495);
#10673=AXIS2_PLACEMENT_3D('',#16594,#13500,#13501);
#10674=AXIS2_PLACEMENT_3D('',#16600,#13505,#13506);
#10675=AXIS2_PLACEMENT_3D('',#16606,#13510,#13511);
#10676=AXIS2_PLACEMENT_3D('',#16612,#13515,#13516);
#10677=AXIS2_PLACEMENT_3D('',#16618,#13520,#13521);
#10678=AXIS2_PLACEMENT_3D('',#16621,#13524,#13525);
#10679=AXIS2_PLACEMENT_3D('',#16622,#13526,#13527);
#10680=AXIS2_PLACEMENT_3D('',#16624,#13528,#13529);
#10681=AXIS2_PLACEMENT_3D('',#16625,#13530,#13531);
#10682=AXIS2_PLACEMENT_3D('',#16627,#13532,#13533);
#10683=AXIS2_PLACEMENT_3D('',#16629,#13535,#13536);
#10684=AXIS2_PLACEMENT_3D('',#16631,#13537,#13538);
#10685=AXIS2_PLACEMENT_3D('',#16633,#13540,#13541);
#10686=AXIS2_PLACEMENT_3D('',#16635,#13542,#13543);
#10687=AXIS2_PLACEMENT_3D('',#16637,#13545,#13546);
#13492=DIRECTION('axis',(0.,0.,1.));
#13493=DIRECTION('refdir',(1.,0.,0.));
#13494=DIRECTION('center_axis',(0.866025403784439,0.,-0.5));
#13495=DIRECTION('ref_axis',(0.5,0.,0.866025403784439));
#13496=DIRECTION('',(0.5,0.,0.866025403784439));
#13497=DIRECTION('',(0.,-1.,0.));
#13498=DIRECTION('',(0.5,0.,0.866025403784439));
#13499=DIRECTION('',(0.,-1.,0.));
#13500=DIRECTION('center_axis',(1.20185167898973E-16,0.,-1.));
#13501=DIRECTION('ref_axis',(1.,0.,1.20185167898973E-16));
#13502=DIRECTION('',(1.,0.,1.20185167898973E-16));
#13503=DIRECTION('',(0.,-1.,0.));
#13504=DIRECTION('',(1.,0.,1.20185167898973E-16));
#13505=DIRECTION('center_axis',(-0.866025403784439,0.,-0.5));
#13506=DIRECTION('ref_axis',(0.5,0.,-0.866025403784439));
#13507=DIRECTION('',(0.5,0.,-0.866025403784439));
#13508=DIRECTION('',(0.,-1.,0.));
#13509=DIRECTION('',(0.5,0.,-0.866025403784439));
#13510=DIRECTION('center_axis',(-0.866025403784439,0.,0.5));
#13511=DIRECTION('ref_axis',(-0.5,0.,-0.866025403784439));
#13512=DIRECTION('',(-0.5,0.,-0.866025403784439));
#13513=DIRECTION('',(0.,-1.,0.));
#13514=DIRECTION('',(-0.5,0.,-0.866025403784439));
#13515=DIRECTION('center_axis',(-2.40370335797945E-16,0.,1.));
#13516=DIRECTION('ref_axis',(-1.,0.,-2.40370335797945E-16));
#13517=DIRECTION('',(-1.,0.,-2.40370335797945E-16));
#13518=DIRECTION('',(0.,-1.,0.));
#13519=DIRECTION('',(-1.,0.,-2.40370335797945E-16));
#13520=DIRECTION('center_axis',(0.866025403784439,0.,0.5));
#13521=DIRECTION('ref_axis',(-0.5,0.,0.866025403784439));
#13522=DIRECTION('',(-0.5,0.,0.866025403784439));
#13523=DIRECTION('',(-0.5,0.,0.866025403784439));
#13524=DIRECTION('center_axis',(0.,-1.,0.));
#13525=DIRECTION('ref_axis',(0.,0.,-1.));
#13526=DIRECTION('center_axis',(0.,1.,0.));
#13527=DIRECTION('ref_axis',(0.,0.,1.));
#13528=DIRECTION('center_axis',(0.,-1.,0.));
#13529=DIRECTION('ref_axis',(1.,0.,0.));
#13530=DIRECTION('center_axis',(0.,-1.,0.));
#13531=DIRECTION('ref_axis',(1.,0.,0.));
#13532=DIRECTION('center_axis',(0.,-1.,0.));
#13533=DIRECTION('ref_axis',(1.,0.,0.));
#13534=DIRECTION('',(0.707106781186548,0.707106781186547,8.65956056235494E-17));
#13535=DIRECTION('center_axis',(0.,-1.,0.));
#13536=DIRECTION('ref_axis',(1.,0.,0.));
#13537=DIRECTION('center_axis',(0.,1.,0.));
#13538=DIRECTION('ref_axis',(1.,0.,0.));
#13539=DIRECTION('',(0.,1.,0.));
#13540=DIRECTION('center_axis',(0.,1.,0.));
#13541=DIRECTION('ref_axis',(1.,0.,0.));
#13542=DIRECTION('center_axis',(0.,-1.,0.));
#13543=DIRECTION('ref_axis',(1.,0.,0.));
#13544=DIRECTION('',(-0.707106781186548,0.707106781186547,-8.65956056235494E-17));
#13545=DIRECTION('center_axis',(0.,-1.,0.));
#13546=DIRECTION('ref_axis',(0.,0.,-1.));
#16584=CARTESIAN_POINT('',(0.,0.,0.));
#16585=CARTESIAN_POINT('Origin',(0.0577350269189626,0.,-0.1));
#16586=CARTESIAN_POINT('',(0.0577350269189626,0.,-0.1));
#16587=CARTESIAN_POINT('',(0.115470053837925,0.,0.));
#16588=CARTESIAN_POINT('',(0.0934187836487032,0.,-0.0381939203391614));
#16589=CARTESIAN_POINT('',(0.0577350269189626,-0.2,-0.1));
#16590=CARTESIAN_POINT('',(0.0577350269189626,0.,-0.1));
#16591=CARTESIAN_POINT('',(0.115470053837925,-0.2,0.));
#16592=CARTESIAN_POINT('',(0.115470053837925,-0.2,0.));
#16593=CARTESIAN_POINT('',(0.115470053837925,0.,0.));
#16594=CARTESIAN_POINT('Origin',(-0.0577350269189626,0.,-0.1));
#16595=CARTESIAN_POINT('',(-0.0577350269189626,0.,-0.1));
#16596=CARTESIAN_POINT('',(0.0561324865405187,0.,-0.1));
#16597=CARTESIAN_POINT('',(-0.0577350269189626,-0.2,-0.1));
#16598=CARTESIAN_POINT('',(-0.0577350269189626,0.,-0.1));
#16599=CARTESIAN_POINT('',(0.0577350269189626,-0.2,-0.1));
#16600=CARTESIAN_POINT('Origin',(-0.115470053837925,0.,-1.38777878078145E-17));
#16601=CARTESIAN_POINT('',(-0.115470053837925,0.,-1.41410031829988E-17));
#16602=CARTESIAN_POINT('',(-0.0797862971081845,0.,-0.0618060796608387));
#16603=CARTESIAN_POINT('',(-0.115470053837925,-0.2,-1.38777878078145E-17));
#16604=CARTESIAN_POINT('',(-0.115470053837925,0.,-1.41410031829988E-17));
#16605=CARTESIAN_POINT('',(-0.0577350269189626,-0.2,-0.1));
#16606=CARTESIAN_POINT('Origin',(-0.0577350269189626,0.,0.1));
#16607=CARTESIAN_POINT('',(-0.0577350269189626,0.,0.1));
#16608=CARTESIAN_POINT('',(-0.0509187836487033,0.,0.111806079660839));
#16609=CARTESIAN_POINT('',(-0.0577350269189626,-0.2,0.1));
#16610=CARTESIAN_POINT('',(-0.0577350269189626,0.,0.1));
#16611=CARTESIAN_POINT('',(-0.115470053837925,-0.2,-1.41410031829988E-17));
#16612=CARTESIAN_POINT('Origin',(0.0577350269189626,0.,0.1));
#16613=CARTESIAN_POINT('',(0.0577350269189626,0.,0.1));
#16614=CARTESIAN_POINT('',(0.113867513459481,0.,0.1));
#16615=CARTESIAN_POINT('',(0.0577350269189626,-0.2,0.1));
#16616=CARTESIAN_POINT('',(0.0577350269189626,0.,0.1));
#16617=CARTESIAN_POINT('',(-0.0577350269189626,-0.2,0.1));
#16618=CARTESIAN_POINT('Origin',(0.115470053837925,0.,0.));
#16619=CARTESIAN_POINT('',(0.122286297108185,0.,-0.0118060796608386));
#16620=CARTESIAN_POINT('',(0.0577350269189626,-0.2,0.1));
#16621=CARTESIAN_POINT('Origin',(0.,-0.2,0.));
#16622=CARTESIAN_POINT('Origin',(0.17,0.,0.));
#16623=CARTESIAN_POINT('',(-0.17,-8.67361737988404E-18,-2.0818995585505E-17));
#16624=CARTESIAN_POINT('Origin',(0.,0.,0.));
#16625=CARTESIAN_POINT('Origin',(0.,-0.015,0.));
#16626=CARTESIAN_POINT('',(-0.1954,-0.0254,-2.39295984553393E-17));
#16627=CARTESIAN_POINT('Origin',(0.,-0.0254,0.));
#16628=CARTESIAN_POINT('',(-0.185,-0.015,-2.2655965784226E-17));
#16629=CARTESIAN_POINT('Origin',(0.,-0.2775,0.));
#16630=CARTESIAN_POINT('',(-0.1954,-0.5296,2.39295984553393E-17));
#16631=CARTESIAN_POINT('Origin',(0.,-0.5296,0.));
#16632=CARTESIAN_POINT('',(-0.1954,-0.2775,-2.39295984553393E-17));
#16633=CARTESIAN_POINT('Origin',(0.,-0.5625,0.));
#16634=CARTESIAN_POINT('',(-0.125,-0.6,-1.53080849893419E-17));
#16635=CARTESIAN_POINT('Origin',(0.,-0.6,0.));
#16636=CARTESIAN_POINT('',(-0.1625,-0.5625,-1.99005104861445E-17));
#16637=CARTESIAN_POINT('Origin',(0.,-0.6,0.));
#16749=UNCERTAINTY_MEASURE_WITH_UNIT(LENGTH_MEASURE(0.001),#16800,
'DISTANCE_ACCURACY_VALUE',
'Maximum model space distance between geometric entities at asserted c
onnectivities');
#16750=UNCERTAINTY_MEASURE_WITH_UNIT(LENGTH_MEASURE(0.001),#16800,
'DISTANCE_ACCURACY_VALUE',
'Maximum model space distance between geometric entities at asserted c
onnectivities');
#16798=(
GEOMETRIC_REPRESENTATION_CONTEXT(3)
GLOBAL_UNCERTAINTY_ASSIGNED_CONTEXT((#16749))
GLOBAL_UNIT_ASSIGNED_CONTEXT((#16800,#16802,#16803))
REPRESENTATION_CONTEXT('','3D')
);
#16799=(
GEOMETRIC_REPRESENTATION_CONTEXT(3)
GLOBAL_UNCERTAINTY_ASSIGNED_CONTEXT((#16750))
GLOBAL_UNIT_ASSIGNED_CONTEXT((#16800,#16802,#16803))
REPRESENTATION_CONTEXT('','3D')
);
#16800=(
LENGTH_UNIT()
NAMED_UNIT(*)
SI_UNIT(.CENTI.,.METRE.)
);
#16802=(
NAMED_UNIT(*)
PLANE_ANGLE_UNIT()
SI_UNIT($,.RADIAN.)
);
#16803=(
NAMED_UNIT(*)
SI_UNIT($,.STERADIAN.)
SOLID_ANGLE_UNIT()
);
#16851=SHAPE_DEFINITION_REPRESENTATION(#16948,#17060);
#16948=PRODUCT_DEFINITION_SHAPE('',$,#17109);
#17060=SHAPE_REPRESENTATION('',(#10671),#16798);
#17061=PRODUCT_DEFINITION_CONTEXT('part definition',#17207,'design');
#17109=PRODUCT_DEFINITION('Socket Set Screw - M4x6',
'Socket Set Screw - M4x6',#17157,#17061);
#17157=PRODUCT_DEFINITION_FORMATION('',$,#17256);
#17207=APPLICATION_CONTEXT(
'Core Data for Automotive Mechanical Design Process');
#17208=PRODUCT_CONTEXT('part definition',#17207,'mechanical');
#17256=PRODUCT('Socket Set Screw - M4x6','Socket Set Screw - M4x6',
'Socket Set Screw - M4x6',(#17208));
#17327=COLOUR_RGB('Black',0.12,0.14,0.17);
#17328=FILL_AREA_STYLE_COLOUR('',#17327);
#17329=FILL_AREA_STYLE('',(#17328));
#17330=SURFACE_STYLE_FILL_AREA(#17329);
#17331=SURFACE_SIDE_STYLE('',(#17330));
#17332=SURFACE_STYLE_USAGE(.BOTH.,#17331);
#17333=PRESENTATION_STYLE_ASSIGNMENT((#17332));
ENDSEC;
END-ISO-10303-21;
